ISO-10303-21;
HEADER;
/* Generated by software containing ST-Developer
 * from STEP Tools, Inc. (www.steptools.com) 
 */

FILE_DESCRIPTION(
/* description */ ('Wall-mounted air drop station'),
/* implementation_level */ '2;1');

FILE_NAME(
/* name */ 'M4x10 Cap Screw.step',
/* time_stamp */ '2026-10-28T22:16:19-07:00',
/* author */ (''),
/* organization */ (''),
/* preprocessor_version */ 'ST-DEVELOPER v20.2',
/* originating_system */ 'Autodesk Translation Framework v15.17.0.0',
/* authorisation */ '');

FILE_SCHEMA (('AUTOMOTIVE_DESIGN { 1 0 10303 214 3 1 1 }'));
ENDSEC;

DATA;
#10=MECHANICAL_DESIGN_GEOMETRIC_PRESENTATION_REPRESENTATION('',(#372),#10517);
#253=ORIENTED_CLOSED_SHELL('',*,#5913,.F.);
#256=BREP_WITH_VOIDS('Body1',#5914,(#253));
#283=CONICAL_SURFACE('',#6905,0.325,0.785398163397448);
#284=CONICAL_SURFACE('',#6909,0.335,0.785398163397448);
#285=CONICAL_SURFACE('',#6913,0.21,0.463647609000806);
#314=SHAPE_REPRESENTATION_RELATIONSHIP('SRR','None',#10672,#343);
#343=ADVANCED_BREP_SHAPE_REPRESENTATION('',(#256),#10516);
#372=STYLED_ITEM('',(#10881),#256);
#525=FACE_BOUND('',#1589,.T.);
#744=PLANE('',#6893);
#745=PLANE('',#6894);
#746=PLANE('',#6895);
#747=PLANE('',#6896);
#748=PLANE('',#6897);
#749=PLANE('',#6898);
#750=PLANE('',#6899);
#751=PLANE('',#6900);
#752=PLANE('',#6901);
#753=PLANE('',#6903);
#754=PLANE('',#6911);
#1094=FACE_OUTER_BOUND('',#1575,.T.);
#1095=FACE_OUTER_BOUND('',#1576,.T.);
#1096=FACE_OUTER_BOUND('',#1577,.T.);
#1097=FACE_OUTER_BOUND('',#1578,.T.);
#1098=FACE_OUTER_BOUND('',#1579,.T.);
#1099=FACE_OUTER_BOUND('',#1580,.T.);
#1100=FACE_OUTER_BOUND('',#1581,.T.);
#1101=FACE_OUTER_BOUND('',#1582,.T.);
#1102=FACE_OUTER_BOUND('',#1583,.T.);
#1103=FACE_OUTER_BOUND('',#1584,.T.);
#1104=FACE_OUTER_BOUND('',#1585,.T.);
#1105=FACE_OUTER_BOUND('',#1586,.T.);
#1106=FACE_OUTER_BOUND('',#1587,.T.);
#1107=FACE_OUTER_BOUND('',#1588,.T.);
#1108=FACE_OUTER_BOUND('',#1590,.T.);
#1109=FACE_OUTER_BOUND('',#1591,.T.);
#1575=EDGE_LOOP('',(#5371,#5372,#5373,#5374));
#1576=EDGE_LOOP('',(#5375,#5376,#5377,#5378));
#1577=EDGE_LOOP('',(#5379,#5380,#5381,#5382));
#1578=EDGE_LOOP('',(#5383,#5384,#5385,#5386));
#1579=EDGE_LOOP('',(#5387,#5388,#5389,#5390));
#1580=EDGE_LOOP('',(#5391,#5392,#5393,#5394));
#1581=EDGE_LOOP('',(#5395,#5396,#5397,#5398,#5399,#5400));
#1582=EDGE_LOOP('',(#5401,#5402,#5403,#5404,#5405,#5406));
#1583=EDGE_LOOP('',(#5407));
#1584=EDGE_LOOP('',(#5408));
#1585=EDGE_LOOP('',(#5409,#5410,#5411,#5412));
#1586=EDGE_LOOP('',(#5413,#5414,#5415,#5416));
#1587=EDGE_LOOP('',(#5417,#5418,#5419,#5420));
#1588=EDGE_LOOP('',(#5421));
#1589=EDGE_LOOP('',(#5422));
#1590=EDGE_LOOP('',(#5423,#5424,#5425,#5426));
#1591=EDGE_LOOP('',(#5427,#5428,#5429,#5430));
#2033=LINE('',#10382,#2497);
#2034=LINE('',#10384,#2498);
#2035=LINE('',#10386,#2499);
#2036=LINE('',#10387,#2500);
#2037=LINE('',#10390,#2501);
#2038=LINE('',#10392,#2502);
#2039=LINE('',#10393,#2503);
#2040=LINE('',#10396,#2504);
#2041=LINE('',#10398,#2505);
#2042=LINE('',#10399,#2506);
#2043=LINE('',#10402,#2507);
#2044=LINE('',#10404,#2508);
#2045=LINE('',#10405,#2509);
#2046=LINE('',#10408,#2510);
#2047=LINE('',#10410,#2511);
#2048=LINE('',#10411,#2512);
#2049=LINE('',#10413,#2513);
#2050=LINE('',#10414,#2514);
#2051=LINE('',#10426,#2515);
#2052=LINE('',#10430,#2516);
#2053=LINE('',#10434,#2517);
#2054=LINE('',#10441,#2518);
#2055=LINE('',#10443,#2519);
#2497=VECTOR('',#8683,1.);
#2498=VECTOR('',#8684,1.);
#2499=VECTOR('',#8685,1.);
#2500=VECTOR('',#8686,1.);
#2501=VECTOR('',#8689,1.);
#2502=VECTOR('',#8690,1.);
#2503=VECTOR('',#8691,1.);
#2504=VECTOR('',#8694,1.);
#2505=VECTOR('',#8695,1.);
#2506=VECTOR('',#8696,1.);
#2507=VECTOR('',#8699,1.);
#2508=VECTOR('',#8700,1.);
#2509=VECTOR('',#8701,1.);
#2510=VECTOR('',#8704,1.);
#2511=VECTOR('',#8705,1.);
#2512=VECTOR('',#8706,1.);
#2513=VECTOR('',#8709,1.);
#2514=VECTOR('',#8710,1.);
#2515=VECTOR('',#8727,0.325);
#2516=VECTOR('',#8732,0.35);
#2517=VECTOR('',#8737,0.335);
#2518=VECTOR('',#8746,0.21);
#2519=VECTOR('',#8749,0.2);
#2758=CIRCLE('',#6902,0.1954);
#2759=CIRCLE('',#6904,0.3);
#2760=CIRCLE('',#6906,0.35);
#2761=CIRCLE('',#6908,0.35);
#2762=CIRCLE('',#6910,0.32);
#2763=CIRCLE('',#6912,0.22);
#2764=CIRCLE('',#6914,0.1954);
#3225=VERTEX_POINT('',#10380);
#3226=VERTEX_POINT('',#10381);
#3227=VERTEX_POINT('',#10383);
#3228=VERTEX_POINT('',#10385);
#3229=VERTEX_POINT('',#10389);
#3230=VERTEX_POINT('',#10391);
#3231=VERTEX_POINT('',#10395);
#3232=VERTEX_POINT('',#10397);
#3233=VERTEX_POINT('',#10401);
#3234=VERTEX_POINT('',#10403);
#3235=VERTEX_POINT('',#10407);
#3236=VERTEX_POINT('',#10409);
#3237=VERTEX_POINT('',#10418);
#3238=VERTEX_POINT('',#10421);
#3239=VERTEX_POINT('',#10424);
#3240=VERTEX_POINT('',#10428);
#3241=VERTEX_POINT('',#10432);
#3242=VERTEX_POINT('',#10436);
#3243=VERTEX_POINT('',#10439);
#3943=EDGE_CURVE('',#3225,#3226,#2033,.T.);
#3944=EDGE_CURVE('',#3226,#3227,#2034,.T.);
#3945=EDGE_CURVE('',#3227,#3228,#2035,.T.);
#3946=EDGE_CURVE('',#3225,#3228,#2036,.T.);
#3947=EDGE_CURVE('',#3226,#3229,#2037,.T.);
#3948=EDGE_CURVE('',#3229,#3230,#2038,.T.);
#3949=EDGE_CURVE('',#3230,#3227,#2039,.T.);
#3950=EDGE_CURVE('',#3229,#3231,#2040,.T.);
#3951=EDGE_CURVE('',#3231,#3232,#2041,.T.);
#3952=EDGE_CURVE('',#3232,#3230,#2042,.T.);
#3953=EDGE_CURVE('',#3231,#3233,#2043,.T.);
#3954=EDGE_CURVE('',#3233,#3234,#2044,.T.);
#3955=EDGE_CURVE('',#3234,#3232,#2045,.T.);
#3956=EDGE_CURVE('',#3233,#3235,#2046,.T.);
#3957=EDGE_CURVE('',#3235,#3236,#2047,.T.);
#3958=EDGE_CURVE('',#3236,#3234,#2048,.T.);
#3959=EDGE_CURVE('',#3235,#3225,#2049,.T.);
#3960=EDGE_CURVE('',#3228,#3236,#2050,.T.);
#3961=EDGE_CURVE('',#3237,#3237,#2758,.T.);
#3962=EDGE_CURVE('',#3238,#3238,#2759,.T.);
#3963=EDGE_CURVE('',#3239,#3239,#2760,.T.);
#3964=EDGE_CURVE('',#3239,#3238,#2051,.T.);
#3965=EDGE_CURVE('',#3240,#3240,#2761,.T.);
#3966=EDGE_CURVE('',#3240,#3239,#2052,.T.);
#3967=EDGE_CURVE('',#3241,#3241,#2762,.T.);
#3968=EDGE_CURVE('',#3241,#3240,#2053,.T.);
#3969=EDGE_CURVE('',#3242,#3242,#2763,.T.);
#3970=EDGE_CURVE('',#3243,#3243,#2764,.F.);
#3971=EDGE_CURVE('',#3243,#3242,#2054,.T.);
#3972=EDGE_CURVE('',#3237,#3243,#2055,.T.);
#5371=ORIENTED_EDGE('',*,*,#3943,.T.);
#5372=ORIENTED_EDGE('',*,*,#3944,.T.);
#5373=ORIENTED_EDGE('',*,*,#3945,.T.);
#5374=ORIENTED_EDGE('',*,*,#3946,.F.);
#5375=ORIENTED_EDGE('',*,*,#3947,.T.);
#5376=ORIENTED_EDGE('',*,*,#3948,.T.);
#5377=ORIENTED_EDGE('',*,*,#3949,.T.);
#5378=ORIENTED_EDGE('',*,*,#3944,.F.);
#5379=ORIENTED_EDGE('',*,*,#3950,.T.);
#5380=ORIENTED_EDGE('',*,*,#3951,.T.);
#5381=ORIENTED_EDGE('',*,*,#3952,.T.);
#5382=ORIENTED_EDGE('',*,*,#3948,.F.);
#5383=ORIENTED_EDGE('',*,*,#3953,.T.);
#5384=ORIENTED_EDGE('',*,*,#3954,.T.);
#5385=ORIENTED_EDGE('',*,*,#3955,.T.);
#5386=ORIENTED_EDGE('',*,*,#3951,.F.);
#5387=ORIENTED_EDGE('',*,*,#3956,.T.);
#5388=ORIENTED_EDGE('',*,*,#3957,.T.);
#5389=ORIENTED_EDGE('',*,*,#3958,.T.);
#5390=ORIENTED_EDGE('',*,*,#3954,.F.);
#5391=ORIENTED_EDGE('',*,*,#3959,.T.);
#5392=ORIENTED_EDGE('',*,*,#3946,.T.);
#5393=ORIENTED_EDGE('',*,*,#3960,.T.);
#5394=ORIENTED_EDGE('',*,*,#3957,.F.);
#5395=ORIENTED_EDGE('',*,*,#3959,.F.);
#5396=ORIENTED_EDGE('',*,*,#3956,.F.);
#5397=ORIENTED_EDGE('',*,*,#3953,.F.);
#5398=ORIENTED_EDGE('',*,*,#3950,.F.);
#5399=ORIENTED_EDGE('',*,*,#3947,.F.);
#5400=ORIENTED_EDGE('',*,*,#3943,.F.);
#5401=ORIENTED_EDGE('',*,*,#3960,.F.);
#5402=ORIENTED_EDGE('',*,*,#3945,.F.);
#5403=ORIENTED_EDGE('',*,*,#3949,.F.);
#5404=ORIENTED_EDGE('',*,*,#3952,.F.);
#5405=ORIENTED_EDGE('',*,*,#3955,.F.);
#5406=ORIENTED_EDGE('',*,*,#3958,.F.);
#5407=ORIENTED_EDGE('',*,*,#3961,.F.);
#5408=ORIENTED_EDGE('',*,*,#3962,.F.);
#5409=ORIENTED_EDGE('',*,*,#3963,.F.);
#5410=ORIENTED_EDGE('',*,*,#3964,.T.);
#5411=ORIENTED_EDGE('',*,*,#3962,.T.);
#5412=ORIENTED_EDGE('',*,*,#3964,.F.);
#5413=ORIENTED_EDGE('',*,*,#3965,.F.);
#5414=ORIENTED_EDGE('',*,*,#3966,.T.);
#5415=ORIENTED_EDGE('',*,*,#3963,.T.);
#5416=ORIENTED_EDGE('',*,*,#3966,.F.);
#5417=ORIENTED_EDGE('',*,*,#3967,.F.);
#5418=ORIENTED_EDGE('',*,*,#3968,.T.);
#5419=ORIENTED_EDGE('',*,*,#3965,.T.);
#5420=ORIENTED_EDGE('',*,*,#3968,.F.);
#5421=ORIENTED_EDGE('',*,*,#3967,.T.);
#5422=ORIENTED_EDGE('',*,*,#3969,.F.);
#5423=ORIENTED_EDGE('',*,*,#3970,.F.);
#5424=ORIENTED_EDGE('',*,*,#3971,.T.);
#5425=ORIENTED_EDGE('',*,*,#3969,.T.);
#5426=ORIENTED_EDGE('',*,*,#3971,.F.);
#5427=ORIENTED_EDGE('',*,*,#3961,.T.);
#5428=ORIENTED_EDGE('',*,*,#3972,.T.);
#5429=ORIENTED_EDGE('',*,*,#3970,.T.);
#5430=ORIENTED_EDGE('',*,*,#3972,.F.);
#5526=CYLINDRICAL_SURFACE('',#6907,0.35);
#5527=CYLINDRICAL_SURFACE('',#6915,0.1954);
#5867=ADVANCED_FACE('',(#1094),#744,.F.);
#5868=ADVANCED_FACE('',(#1095),#745,.F.);
#5869=ADVANCED_FACE('',(#1096),#746,.F.);
#5870=ADVANCED_FACE('',(#1097),#747,.F.);
#5871=ADVANCED_FACE('',(#1098),#748,.F.);
#5872=ADVANCED_FACE('',(#1099),#749,.F.);
#5873=ADVANCED_FACE('',(#1100),#750,.F.);
#5874=ADVANCED_FACE('',(#1101),#751,.F.);
#5875=ADVANCED_FACE('',(#1102),#752,.F.);
#5876=ADVANCED_FACE('',(#1103),#753,.T.);
#5877=ADVANCED_FACE('',(#1104),#283,.T.);
#5878=ADVANCED_FACE('',(#1105),#5526,.T.);
#5879=ADVANCED_FACE('',(#1106),#284,.T.);
#5880=ADVANCED_FACE('',(#1107,#525),#754,.T.);
#5881=ADVANCED_FACE('',(#1108),#285,.T.);
#5882=ADVANCED_FACE('',(#1109),#5527,.T.);
#5913=CLOSED_SHELL('',(#5867,#5868,#5869,#5870,#5871,#5872,#5873,#5874));
#5914=CLOSED_SHELL('',(#5875,#5876,#5877,#5878,#5879,#5880,#5881,#5882));
#6892=AXIS2_PLACEMENT_3D('',#10378,#8679,#8680);
#6893=AXIS2_PLACEMENT_3D('',#10379,#8681,#8682);
#6894=AXIS2_PLACEMENT_3D('',#10388,#8687,#8688);
#6895=AXIS2_PLACEMENT_3D('',#10394,#8692,#8693);
#6896=AXIS2_PLACEMENT_3D('',#10400,#8697,#8698);
#6897=AXIS2_PLACEMENT_3D('',#10406,#8702,#8703);
#6898=AXIS2_PLACEMENT_3D('',#10412,#8707,#8708);
#6899=AXIS2_PLACEMENT_3D('',#10415,#8711,#8712);
#6900=AXIS2_PLACEMENT_3D('',#10416,#8713,#8714);
#6901=AXIS2_PLACEMENT_3D('',#10417,#8715,#8716);
#6902=AXIS2_PLACEMENT_3D('',#10419,#8717,#8718);
#6903=AXIS2_PLACEMENT_3D('',#10420,#8719,#8720);
#6904=AXIS2_PLACEMENT_3D('',#10422,#8721,#8722);
#6905=AXIS2_PLACEMENT_3D('',#10423,#8723,#8724);
#6906=AXIS2_PLACEMENT_3D('',#10425,#8725,#8726);
#6907=AXIS2_PLACEMENT_3D('',#10427,#8728,#8729);
#6908=AXIS2_PLACEMENT_3D('',#10429,#8730,#8731);
#6909=AXIS2_PLACEMENT_3D('',#10431,#8733,#8734);
#6910=AXIS2_PLACEMENT_3D('',#10433,#8735,#8736);
#6911=AXIS2_PLACEMENT_3D('',#10435,#8738,#8739);
#6912=AXIS2_PLACEMENT_3D('',#10437,#8740,#8741);
#6913=AXIS2_PLACEMENT_3D('',#10438,#8742,#8743);
#6914=AXIS2_PLACEMENT_3D('',#10440,#8744,#8745);
#6915=AXIS2_PLACEMENT_3D('',#10442,#8747,#8748);
#8679=DIRECTION('axis',(0.,0.,1.));
#8680=DIRECTION('refdir',(1.,0.,0.));
#8681=DIRECTION('center_axis',(0.866025403784439,0.,-0.5));
#8682=DIRECTION('ref_axis',(0.5,0.,0.866025403784439));
#8683=DIRECTION('',(-0.5,0.,-0.866025403784439));
#8684=DIRECTION('',(0.,-1.,0.));
#8685=DIRECTION('',(0.5,0.,0.866025403784439));
#8686=DIRECTION('',(0.,-1.,0.));
#8687=DIRECTION('center_axis',(1.60246890531964E-16,0.,-1.));
#8688=DIRECTION('ref_axis',(1.,0.,1.60246890531964E-16));
#8689=DIRECTION('',(-1.,0.,-1.60246890531964E-16));
#8690=DIRECTION('',(0.,-1.,0.));
#8691=DIRECTION('',(1.,0.,1.60246890531964E-16));
#8692=DIRECTION('center_axis',(-0.866025403784439,0.,-0.5));
#8693=DIRECTION('ref_axis',(0.5,0.,-0.866025403784439));
#8694=DIRECTION('',(-0.5,0.,0.866025403784439));
#8695=DIRECTION('',(0.,-1.,0.));
#8696=DIRECTION('',(0.5,0.,-0.866025403784439));
#8697=DIRECTION('center_axis',(-0.866025403784439,0.,0.5));
#8698=DIRECTION('ref_axis',(-0.5,0.,-0.866025403784439));
#8699=DIRECTION('',(0.5,0.,0.866025403784439));
#8700=DIRECTION('',(0.,-1.,0.));
#8701=DIRECTION('',(-0.5,0.,-0.866025403784439));
#8702=DIRECTION('center_axis',(-1.60246890531964E-16,0.,1.));
#8703=DIRECTION('ref_axis',(-1.,0.,-1.60246890531964E-16));
#8704=DIRECTION('',(1.,0.,1.60246890531964E-16));
#8705=DIRECTION('',(0.,-1.,0.));
#8706=DIRECTION('',(-1.,0.,-1.60246890531964E-16));
#8707=DIRECTION('center_axis',(0.866025403784439,0.,0.5));
#8708=DIRECTION('ref_axis',(-0.5,0.,0.866025403784439));
#8709=DIRECTION('',(0.5,0.,-0.866025403784439));
#8710=DIRECTION('',(-0.5,0.,0.866025403784439));
#8711=DIRECTION('center_axis',(0.,1.,0.));
#8712=DIRECTION('ref_axis',(1.,0.,0.));
#8713=DIRECTION('center_axis',(0.,-1.,0.));
#8714=DIRECTION('ref_axis',(0.,0.,-1.));
#8715=DIRECTION('center_axis',(0.,1.,0.));
#8716=DIRECTION('ref_axis',(1.,0.,0.));
#8717=DIRECTION('center_axis',(0.,1.,0.));
#8718=DIRECTION('ref_axis',(1.,0.,0.));
#8719=DIRECTION('center_axis',(0.,1.,0.));
#8720=DIRECTION('ref_axis',(0.,0.,1.));
#8721=DIRECTION('center_axis',(0.,-1.,0.));
#8722=DIRECTION('ref_axis',(1.,0.,0.));
#8723=DIRECTION('center_axis',(0.,-1.,0.));
#8724=DIRECTION('ref_axis',(1.,0.,0.));
#8725=DIRECTION('center_axis',(0.,-1.,0.));
#8726=DIRECTION('ref_axis',(1.,0.,0.));
#8727=DIRECTION('',(0.707106781186547,0.707106781186548,8.65956056235493E-17));
#8728=DIRECTION('center_axis',(0.,-1.,0.));
#8729=DIRECTION('ref_axis',(1.,0.,0.));
#8730=DIRECTION('center_axis',(0.,-1.,0.));
#8731=DIRECTION('ref_axis',(1.,0.,0.));
#8732=DIRECTION('',(0.,1.,0.));
#8733=DIRECTION('center_axis',(0.,1.,0.));
#8734=DIRECTION('ref_axis',(1.,0.,0.));
#8735=DIRECTION('center_axis',(0.,-1.,0.));
#8736=DIRECTION('ref_axis',(1.,0.,0.));
#8737=DIRECTION('',(-0.707106781186547,0.707106781186548,-8.65956056235493E-17));
#8738=DIRECTION('center_axis',(0.,-1.,0.));
#8739=DIRECTION('ref_axis',(0.,0.,-1.));
#8740=DIRECTION('center_axis',(0.,-1.,0.));
#8741=DIRECTION('ref_axis',(1.,0.,0.));
#8742=DIRECTION('center_axis',(0.,1.,0.));
#8743=DIRECTION('ref_axis',(1.,0.,0.));
#8744=DIRECTION('center_axis',(0.,1.,0.));
#8745=DIRECTION('ref_axis',(1.,0.,0.));
#8746=DIRECTION('',(-0.447213595499958,0.894427190999916,-5.47678698264203E-17));
#8747=DIRECTION('center_axis',(0.,-1.,0.));
#8748=DIRECTION('ref_axis',(1.,0.,0.));
#8749=DIRECTION('',(0.,1.,0.));
#10378=CARTESIAN_POINT('',(0.,0.,0.));
#10379=CARTESIAN_POINT('Origin',(0.0866025403784439,-0.4,-0.15));
#10380=CARTESIAN_POINT('',(0.173205080756888,-0.4,0.));
#10381=CARTESIAN_POINT('',(0.0866025403784439,-0.4,-0.15));
#10382=CARTESIAN_POINT('',(0.173205080756888,-0.4,0.));
#10383=CARTESIAN_POINT('',(0.0866025403784439,-0.64,-0.15));
#10384=CARTESIAN_POINT('',(0.0866025403784439,-0.4,-0.15));
#10385=CARTESIAN_POINT('',(0.173205080756888,-0.64,0.));
#10386=CARTESIAN_POINT('',(0.173205080756888,-0.64,0.));
#10387=CARTESIAN_POINT('',(0.173205080756888,-0.4,0.));
#10388=CARTESIAN_POINT('Origin',(-0.0866025403784438,-0.4,-0.15));
#10389=CARTESIAN_POINT('',(-0.0866025403784438,-0.4,-0.15));
#10390=CARTESIAN_POINT('',(0.0866025403784439,-0.4,-0.15));
#10391=CARTESIAN_POINT('',(-0.0866025403784438,-0.64,-0.15));
#10392=CARTESIAN_POINT('',(-0.0866025403784438,-0.4,-0.15));
#10393=CARTESIAN_POINT('',(0.0866025403784439,-0.64,-0.15));
#10394=CARTESIAN_POINT('Origin',(-0.173205080756888,-0.4,-2.77555756156289E-17));
#10395=CARTESIAN_POINT('',(-0.173205080756888,-0.4,-2.12115047744981E-17));
#10396=CARTESIAN_POINT('',(-0.0866025403784438,-0.4,-0.15));
#10397=CARTESIAN_POINT('',(-0.173205080756888,-0.64,-2.77555756156289E-17));
#10398=CARTESIAN_POINT('',(-0.173205080756888,-0.4,-2.12115047744981E-17));
#10399=CARTESIAN_POINT('',(-0.0866025403784438,-0.64,-0.15));
#10400=CARTESIAN_POINT('Origin',(-0.0866025403784439,-0.4,0.15));
#10401=CARTESIAN_POINT('',(-0.0866025403784439,-0.4,0.15));
#10402=CARTESIAN_POINT('',(-0.173205080756888,-0.4,-2.12115047744981E-17));
#10403=CARTESIAN_POINT('',(-0.0866025403784439,-0.64,0.15));
#10404=CARTESIAN_POINT('',(-0.0866025403784439,-0.4,0.15));
#10405=CARTESIAN_POINT('',(-0.173205080756888,-0.64,-2.12115047744981E-17));
#10406=CARTESIAN_POINT('Origin',(0.0866025403784439,-0.4,0.15));
#10407=CARTESIAN_POINT('',(0.0866025403784439,-0.4,0.15));
#10408=CARTESIAN_POINT('',(-0.0866025403784439,-0.4,0.15));
#10409=CARTESIAN_POINT('',(0.0866025403784439,-0.64,0.15));
#10410=CARTESIAN_POINT('',(0.0866025403784439,-0.4,0.15));
#10411=CARTESIAN_POINT('',(-0.0866025403784439,-0.64,0.15));
#10412=CARTESIAN_POINT('Origin',(0.173205080756888,-0.4,0.));
#10413=CARTESIAN_POINT('',(0.0866025403784439,-0.4,0.15));
#10414=CARTESIAN_POINT('',(0.0866025403784439,-0.64,0.15));
#10415=CARTESIAN_POINT('Origin',(0.,-0.4,-2.77555756156289E-17));
#10416=CARTESIAN_POINT('Origin',(0.,-0.64,-2.77555756156289E-17));
#10417=CARTESIAN_POINT('Origin',(0.,-1.,0.));
#10418=CARTESIAN_POINT('',(-0.1954,-1.,2.39295984553393E-17));
#10419=CARTESIAN_POINT('Origin',(0.,-1.,0.));
#10420=CARTESIAN_POINT('Origin',(0.3,0.4,0.));
#10421=CARTESIAN_POINT('',(-0.3,0.4,-3.67394039744206E-17));
#10422=CARTESIAN_POINT('Origin',(0.,0.4,0.));
#10423=CARTESIAN_POINT('Origin',(0.,0.375,0.));
#10424=CARTESIAN_POINT('',(-0.35,0.35,-4.28626379701573E-17));
#10425=CARTESIAN_POINT('Origin',(0.,0.35,0.));
#10426=CARTESIAN_POINT('',(-0.325,0.375,-3.9801020972289E-17));
#10427=CARTESIAN_POINT('Origin',(0.,0.19,0.));
#10428=CARTESIAN_POINT('',(-0.35,0.03,-4.28626379701574E-17));
#10429=CARTESIAN_POINT('Origin',(0.,0.03,0.));
#10430=CARTESIAN_POINT('',(-0.35,0.19,-4.28626379701574E-17));
#10431=CARTESIAN_POINT('Origin',(0.,0.0149999999999999,0.));
#10432=CARTESIAN_POINT('',(-0.32,-3.29597460435593E-17,-3.91886975727153E-17));
#10433=CARTESIAN_POINT('Origin',(0.,0.,0.));
#10434=CARTESIAN_POINT('',(-0.335,0.0149999999999999,-4.10256677714363E-17));
#10435=CARTESIAN_POINT('Origin',(0.22,0.,0.));
#10436=CARTESIAN_POINT('',(-0.22,-6.93889390390723E-18,-2.69422295812418E-17));
#10437=CARTESIAN_POINT('Origin',(0.,0.,0.));
#10438=CARTESIAN_POINT('Origin',(0.,-0.02,0.));
#10439=CARTESIAN_POINT('',(-0.1954,-0.0492,2.39295984553393E-17));
#10440=CARTESIAN_POINT('Origin',(0.,-0.0492,0.));
#10441=CARTESIAN_POINT('',(-0.21,-0.02,-2.57175827820944E-17));
#10442=CARTESIAN_POINT('Origin',(0.,-0.8,0.));
#10443=CARTESIAN_POINT('',(-0.1954,-0.8,-2.39295984553393E-17));
#10483=UNCERTAINTY_MEASURE_WITH_UNIT(LENGTH_MEASURE(0.001),#10518,
'DISTANCE_ACCURACY_VALUE',
'Maximum model space distance between geometric entities at asserted c
onnectivities');
#10484=UNCERTAINTY_MEASURE_WITH_UNIT(LENGTH_MEASURE(0.001),#10518,
'DISTANCE_ACCURACY_VALUE',
'Maximum model space distance between geometric entities at asserted c
onnectivities');
#10516=(
GEOMETRIC_REPRESENTATION_CONTEXT(3)
GLOBAL_UNCERTAINTY_ASSIGNED_CONTEXT((#10483))
GLOBAL_UNIT_ASSIGNED_CONTEXT((#10518,#10520,#10521))
REPRESENTATION_CONTEXT('','3D')
);
#10517=(
GEOMETRIC_REPRESENTATION_CONTEXT(3)
GLOBAL_UNCERTAINTY_ASSIGNED_CONTEXT((#10484))
GLOBAL_UNIT_ASSIGNED_CONTEXT((#10518,#10520,#10521))
REPRESENTATION_CONTEXT('','3D')
);
#10518=(
LENGTH_UNIT()
NAMED_UNIT(*)
SI_UNIT(.CENTI.,.METRE.)
);
#10520=(
NAMED_UNIT(*)
PLANE_ANGLE_UNIT()
SI_UNIT($,.RADIAN.)
);
#10521=(
NAMED_UNIT(*)
SI_UNIT($,.STERADIAN.)
SOLID_ANGLE_UNIT()
);
#10553=SHAPE_DEFINITION_REPRESENTATION(#10632,#10672);
#10632=PRODUCT_DEFINITION_SHAPE('',$,#10705);
#10672=SHAPE_REPRESENTATION('',(#6892),#10516);
#10673=PRODUCT_DEFINITION_CONTEXT('part definition',#10771,'design');
#10705=PRODUCT_DEFINITION('M4x10 Cap Screw','M4x10 Cap Screw',#10737,#10673);
#10737=PRODUCT_DEFINITION_FORMATION('',$,#10804);
#10771=APPLICATION_CONTEXT(
'Core Data for Automotive Mechanical Design Process');
#10772=PRODUCT_CONTEXT('part definition',#10771,'mechanical');
#10804=PRODUCT('M4x10 Cap Screw','M4x10 Cap Screw','M4x10 Cap Screw',(#10772));
#10875=COLOUR_RGB('Black',0.12,0.14,0.17);
#10876=FILL_AREA_STYLE_COLOUR('',#10875);
#10877=FILL_AREA_STYLE('',(#10876));
#10878=SURFACE_STYLE_FILL_AREA(#10877);
#10879=SURFACE_SIDE_STYLE('',(#10878));
#10880=SURFACE_STYLE_USAGE(.BOTH.,#10879);
#10881=PRESENTATION_STYLE_ASSIGNMENT((#10880));
ENDSEC;
END-ISO-10303-21;
